ISO-10303-21;
HEADER;
FILE_DESCRIPTION (('STEP AP214'),
    '1' );
FILE_NAME ('Supporter.step',
    '2026-10-23T20:35:44',
    ( '' ),
    ( '' ),
    'SwSTEP 2.0',
    'SolidWorks 2025',
    '' );
FILE_SCHEMA (( 'AUTOMOTIVE_DESIGN' ));
ENDSEC;

DATA;
#23=SHAPE_REPRESENTATION_RELATIONSHIP ( 'NONE' , 'NONE' ,  #2912, #3774 ) ;
#101=CARTESIAN_POINT ( 'NONE',  ( 2.755905511811024056, 1.496062992125984259, -0.7480314960629921295 ) ) ;
#124=ORIENTED_EDGE ( 'NONE', *, *, #6507, .T. ) ;
#139=VERTEX_POINT ( 'NONE', #316 ) ;
#151=CARTESIAN_POINT ( 'NONE',  ( 1.377952755905512028, 0.7480314960629921295, 0.7480314960629921295 ) ) ;
#155=CYLINDRICAL_SURFACE ( 'NONE', #855, 0.7480314960629921295 ) ;
#173=CIRCLE ( 'NONE', #4442, 0.2362204724409449341 ) ;
#211=CYLINDRICAL_SURFACE ( 'NONE', #635, 0.2362204724409449896 ) ;
#218=ORIENTED_EDGE ( 'NONE', *, *, #3634, .T. ) ;
#250=FACE_OUTER_BOUND ( 'NONE', #326, .T. ) ;
#257=AXIS2_PLACEMENT_3D ( 'NONE', #5618, #942, #371 ) ;
#271=DIRECTION ( 'NONE',  ( -0.000000000000000000, -0.000000000000000000, 1.000000000000000000 ) ) ;
#280=ORIENTED_EDGE ( 'NONE', *, *, #4164, .F. ) ;
#285=LINE ( 'NONE', #398, #6742 ) ;
#316=CARTESIAN_POINT ( 'NONE',  ( 0.9055118110236223261, 0.7480314960629921295, -0.7480314960629921295 ) ) ;
#326=EDGE_LOOP ( 'NONE', ( #3963, #5644, #3881, #5352 ) ) ;
#329=EDGE_CURVE ( 'NONE', #1607, #4990, #5298, .T. ) ;
#360=FACE_OUTER_BOUND ( 'NONE', #1560, .T. ) ;
#371=DIRECTION ( 'NONE',  ( 0.000000000000000000, 0.000000000000000000, 1.000000000000000000 ) ) ;
#386=AXIS2_PLACEMENT_3D ( 'NONE', #757, #3705, #6044 ) ;
#398=CARTESIAN_POINT ( 'NONE',  ( 0.000000000000000000, 1.496062992125984259, 0.7480314960629921295 ) ) ;
#413=DIRECTION ( 'NONE',  ( 1.000000000000000000, 0.000000000000000000, -0.000000000000000000 ) ) ;
#418=CARTESIAN_POINT ( 'NONE',  ( 0.000000000000000000, 0.000000000000000000, 0.000000000000000000 ) ) ;
#420=CARTESIAN_POINT ( 'NONE',  ( 2.892866454678787531E-17, 1.496062992125984259, 0.2362204724409449341 ) ) ;
#432=VECTOR ( 'NONE', #5331, 39.37007874015748143 ) ;
#444=DIRECTION ( 'NONE',  ( 1.000000000000000000, 0.000000000000000000, 0.000000000000000000 ) ) ;
#466=ORIENTED_EDGE ( 'NONE', *, *, #3634, .F. ) ;
#480=PLANE ( 'NONE',  #3038 ) ;
#518=DIRECTION ( 'NONE',  ( 0.000000000000000000, 0.000000000000000000, 1.000000000000000000 ) ) ;
#520=LINE ( 'NONE', #3297, #3400 ) ;
#531=FACE_OUTER_BOUND ( 'NONE', #736, .T. ) ;
#565=EDGE_CURVE ( 'NONE', #7376, #1597, #3596, .T. ) ;
#604=EDGE_CURVE ( 'NONE', #5941, #7498, #3488, .T. ) ;
#609=CIRCLE ( 'NONE', #2560, 0.2362204724409449341 ) ;
#615=ADVANCED_FACE ( 'NONE', ( #3566 ), #1657, .F. ) ;
#624=DIRECTION ( 'NONE',  ( 0.000000000000000000, 0.000000000000000000, 1.000000000000000000 ) ) ;
#635=AXIS2_PLACEMENT_3D ( 'NONE', #7232, #4794, #1411 ) ;
#652=ADVANCED_FACE ( 'NONE', ( #1793, #4134, #5760 ), #3523, .T. ) ;
#696=EDGE_LOOP ( 'NONE', ( #3487, #218 ) ) ;
#723=CARTESIAN_POINT ( 'NONE',  ( 2.755905511811024056, 0.000000000000000000, 0.000000000000000000 ) ) ;
#736=EDGE_LOOP ( 'NONE', ( #7405, #7185, #280, #6307 ) ) ;
#750=LINE ( 'NONE', #6040, #5742 ) ;
#754=PRODUCT_DEFINITION_CONTEXT ( 'detailed design', #2240, 'design' ) ;
#756=CIRCLE ( 'NONE', #6979, 0.2362204724409449341 ) ;
#757=CARTESIAN_POINT ( 'NONE',  ( 2.755905511811024056, 1.496062992125984259, 0.000000000000000000 ) ) ;
#793=EDGE_CURVE ( 'NONE', #1455, #4636, #5492, .T. ) ;
#794=ADVANCED_FACE ( 'NONE', ( #250 ), #211, .F. ) ;
#813=VERTEX_POINT ( 'NONE', #925 ) ;
#825=CIRCLE ( 'NONE', #3885, 0.2362204724409449341 ) ;
#838=DIRECTION ( 'NONE',  ( -0.000000000000000000, -1.000000000000000000, -0.000000000000000000 ) ) ;
#855=AXIS2_PLACEMENT_3D ( 'NONE', #7211, #5510, #4158 ) ;
#879=( GEOMETRIC_REPRESENTATION_CONTEXT ( 3 ) GLOBAL_UNCERTAINTY_ASSIGNED_CONTEXT ( ( #4809 ) ) GLOBAL_UNIT_ASSIGNED_CONTEXT ( ( #5297, #1854, #6527 ) ) REPRESENTATION_CONTEXT ( 'NONE', 'WORKASPACE' ) );
#882=EDGE_CURVE ( 'NONE', #2163, #1804, #285, .T. ) ;
#899=CARTESIAN_POINT ( 'NONE',  ( 2.755905511811024056, 1.496062992125984259, -0.7480314960629921295 ) ) ;
#925=CARTESIAN_POINT ( 'NONE',  ( 0.000000000000000000, 1.496062992125984259, -0.7480314960629921295 ) ) ;
#933=CARTESIAN_POINT ( 'NONE',  ( 0.000000000000000000, 0.000000000000000000, 0.7480314960629921295 ) ) ;
#935=PRODUCT_DEFINITION_FORMATION_WITH_SPECIFIED_SOURCE ( 'ANY', '', #3614, .NOT_KNOWN. ) ;
#942=DIRECTION ( 'NONE',  ( 0.000000000000000000, 1.000000000000000000, 0.000000000000000000 ) ) ;
#944=CYLINDRICAL_SURFACE ( 'NONE', #2080, 0.4724409448818896462 ) ;
#961=CYLINDRICAL_SURFACE ( 'NONE', #4264, 0.2362204724409449341 ) ;
#965=ORIENTED_EDGE ( 'NONE', *, *, #7320, .F. ) ;
#970=LINE ( 'NONE', #6247, #1429 ) ;
#980=FACE_BOUND ( 'NONE', #696, .T. ) ;
#1011=VECTOR ( 'NONE', #271, 39.37007874015748143 ) ;
#1017=DIRECTION ( 'NONE',  ( 0.000000000000000000, 1.000000000000000000, 0.000000000000000000 ) ) ;
#1063=FACE_OUTER_BOUND ( 'NONE', #3751, .T. ) ;
#1078=EDGE_CURVE ( 'NONE', #139, #7188, #6372, .T. ) ;
#1089=AXIS2_PLACEMENT_3D ( 'NONE', #3426, #2167, #413 ) ;
#1114=PLANE ( 'NONE',  #1089 ) ;
#1139=DIRECTION ( 'NONE',  ( -1.000000000000000000, -0.000000000000000000, -0.000000000000000000 ) ) ;
#1175=DIRECTION ( 'NONE',  ( 1.000000000000000000, 0.000000000000000000, 0.000000000000000000 ) ) ;
#1208=VERTEX_POINT ( 'NONE', #3203 ) ;
#1234=CIRCLE ( 'NONE', #6630, 0.2362204724409449896 ) ;
#1271=( CONVERSION_BASED_UNIT ( 'INCH', #1351 ) LENGTH_UNIT ( ) NAMED_UNIT ( #5074 ) );
#1295=ORIENTED_EDGE ( 'NONE', *, *, #5577, .T. ) ;
#1309=AXIS2_PLACEMENT_3D ( 'NONE', #5269, #4619, #4731 ) ;
#1324=CARTESIAN_POINT ( 'NONE',  ( 2.755905511811024056, 1.496062992125984259, 0.000000000000000000 ) ) ;
#1333=VERTEX_POINT ( 'NONE', #420 ) ;
#1351=LENGTH_MEASURE_WITH_UNIT ( LENGTH_MEASURE( 0.02539999999999999897 ), #1769 );
#1364=CARTESIAN_POINT ( 'NONE',  ( 2.755905511811024056, 1.496062992125984259, 0.7480314960629921295 ) ) ;
#1401=ORIENTED_EDGE ( 'NONE', *, *, #3232, .F. ) ;
#1410=ORIENTED_EDGE ( 'NONE', *, *, #5003, .F. ) ;
#1411=DIRECTION ( 'NONE',  ( 0.000000000000000000, 0.000000000000000000, -1.000000000000000000 ) ) ;
#1429=VECTOR ( 'NONE', #5394, 39.37007874015748143 ) ;
#1446=ORIENTED_EDGE ( 'NONE', *, *, #3413, .T. ) ;
#1455=VERTEX_POINT ( 'NONE', #5737 ) ;
#1489=DIRECTION ( 'NONE',  ( 0.000000000000000000, 0.000000000000000000, -1.000000000000000000 ) ) ;
#1494=EDGE_CURVE ( 'NONE', #6698, #4990, #6605, .T. ) ;
#1517=MANIFOLD_SOLID_BREP ( 'Cut-Extrude1', #6528 ) ;
#1540=DIRECTION ( 'NONE',  ( 1.000000000000000000, 0.000000000000000000, 0.000000000000000000 ) ) ;
#1551=CARTESIAN_POINT ( 'NONE',  ( 2.755905511811024056, 1.496062992125984259, -0.2362204724409449896 ) ) ;
#1560=EDGE_LOOP ( 'NONE', ( #6936, #5410, #1956, #5814 ) ) ;
#1565=VERTEX_POINT ( 'NONE', #1622 ) ;
#1597=VERTEX_POINT ( 'NONE', #3493 ) ;
#1607=VERTEX_POINT ( 'NONE', #3647 ) ;
#1622=CARTESIAN_POINT ( 'NONE',  ( 0.000000000000000000, 0.000000000000000000, 0.7480314960629921295 ) ) ;
#1630=CARTESIAN_POINT ( 'NONE',  ( 2.755905511811024056, 0.000000000000000000, 0.000000000000000000 ) ) ;
#1657=CYLINDRICAL_SURFACE ( 'NONE', #4910, 0.4724409448818896462 ) ;
#1659=FACE_BOUND ( 'NONE', #6578, .T. ) ;
#1676=CYLINDRICAL_SURFACE ( 'NONE', #7190, 0.2362204724409449341 ) ;
#1678=DIRECTION ( 'NONE',  ( 0.000000000000000000, 0.000000000000000000, -1.000000000000000000 ) ) ;
#1697=DIRECTION ( 'NONE',  ( 0.000000000000000000, 0.000000000000000000, 1.000000000000000000 ) ) ;
#1722=CARTESIAN_POINT ( 'NONE',  ( 0.000000000000000000, 0.000000000000000000, -0.7480314960629921295 ) ) ;
#1769=( LENGTH_UNIT ( ) NAMED_UNIT ( * ) SI_UNIT ( $, .METRE. ) );
#1793=FACE_BOUND ( 'NONE', #5066, .T. ) ;
#1804=VERTEX_POINT ( 'NONE', #3340 ) ;
#1811=EDGE_CURVE ( 'NONE', #1333, #2767, #2835, .T. ) ;
#1831=DIRECTION ( 'NONE',  ( 0.000000000000000000, 0.000000000000000000, 1.000000000000000000 ) ) ;
#1854=( NAMED_UNIT ( * ) PLANE_ANGLE_UNIT ( ) SI_UNIT ( $, .RADIAN. ) );
#1863=EDGE_CURVE ( 'NONE', #7188, #7376, #520, .T. ) ;
#1909=FACE_OUTER_BOUND ( 'NONE', #3959, .T. ) ;
#1934=CIRCLE ( 'NONE', #1309, 0.4724409448818896462 ) ;
#1956=ORIENTED_EDGE ( 'NONE', *, *, #882, .F. ) ;
#1961=EDGE_CURVE ( 'NONE', #813, #1208, #970, .T. ) ;
#1996=DIRECTION ( 'NONE',  ( -0.000000000000000000, -1.000000000000000000, -0.000000000000000000 ) ) ;
#2022=ADVANCED_FACE ( 'NONE', ( #1909 ), #7213, .F. ) ;
#2048=CARTESIAN_POINT ( 'NONE',  ( 2.755905511811024056, 1.496062992125984259, 0.000000000000000000 ) ) ;
#2062=AXIS2_PLACEMENT_3D ( 'NONE', #1324, #2485, #4202 ) ;
#2072=EDGE_CURVE ( 'NONE', #1804, #1607, #2441, .T. ) ;
#2080=AXIS2_PLACEMENT_3D ( 'NONE', #4998, #4382, #1540 ) ;
#2124=VERTEX_POINT ( 'NONE', #5965 ) ;
#2134=DIRECTION ( 'NONE',  ( 0.000000000000000000, 0.000000000000000000, 1.000000000000000000 ) ) ;
#2156=CARTESIAN_POINT ( 'NONE',  ( 2.892866454678787531E-17, 1.496062992125984259, 0.2362204724409449341 ) ) ;
#2163=VERTEX_POINT ( 'NONE', #4317 ) ;
#2167=DIRECTION ( 'NONE',  ( 0.000000000000000000, 0.000000000000000000, 1.000000000000000000 ) ) ;
#2179=CARTESIAN_POINT ( 'NONE',  ( 1.850393700787401619, 0.7480314960629921295, -0.7480314960629921295 ) ) ;
#2194=ORIENTED_EDGE ( 'NONE', *, *, #5577, .F. ) ;
#2205=CARTESIAN_POINT ( 'NONE',  ( 0.000000000000000000, 0.000000000000000000, 0.000000000000000000 ) ) ;
#2240=APPLICATION_CONTEXT ( 'automotive_design' ) ;
#2247=DIRECTION ( 'NONE',  ( 0.000000000000000000, -0.000000000000000000, 1.000000000000000000 ) ) ;
#2280=ADVANCED_FACE ( 'NONE', ( #5747 ), #961, .F. ) ;
#2310=CARTESIAN_POINT ( 'NONE',  ( 2.755905511811024056, 1.496062992125984259, 0.2362204724409449896 ) ) ;
#2324=ORIENTED_EDGE ( 'NONE', *, *, #4164, .T. ) ;
#2402=ORIENTED_EDGE ( 'NONE', *, *, #3413, .F. ) ;
#2409=CARTESIAN_POINT ( 'NONE',  ( 2.892866454678787531E-17, 0.000000000000000000, 0.2362204724409449341 ) ) ;
#2441=LINE ( 'NONE', #1364, #3154 ) ;
#2485=DIRECTION ( 'NONE',  ( -0.000000000000000000, -1.000000000000000000, -0.000000000000000000 ) ) ;
#2490=ORIENTED_EDGE ( 'NONE', *, *, #6507, .F. ) ;
#2491=DIRECTION ( 'NONE',  ( 1.000000000000000000, 0.000000000000000000, 0.000000000000000000 ) ) ;
#2505=ORIENTED_EDGE ( 'NONE', *, *, #329, .F. ) ;
#2560=AXIS2_PLACEMENT_3D ( 'NONE', #5619, #2696, #2621 ) ;
#2575=ORIENTED_EDGE ( 'NONE', *, *, #6353, .T. ) ;
#2619=AXIS2_PLACEMENT_3D ( 'NONE', #6397, #624, #7003 ) ;
#2621=DIRECTION ( 'NONE',  ( 0.000000000000000000, 0.000000000000000000, 1.000000000000000000 ) ) ;
#2696=DIRECTION ( 'NONE',  ( 0.000000000000000000, 1.000000000000000000, 0.000000000000000000 ) ) ;
#2718=VECTOR ( 'NONE', #2917, 39.37007874015748143 ) ;
#2738=AXIS2_PLACEMENT_3D ( 'NONE', #7059, #6409, #4649 ) ;
#2741=DIRECTION ( 'NONE',  ( 1.000000000000000000, 0.000000000000000000, 0.000000000000000000 ) ) ;
#2753=DIRECTION ( 'NONE',  ( 0.000000000000000000, 0.000000000000000000, 1.000000000000000000 ) ) ;
#2767=VERTEX_POINT ( 'NONE', #2409 ) ;
#2806=ADVANCED_FACE ( 'NONE', ( #1063 ), #1676, .F. ) ;
#2812=CARTESIAN_POINT ( 'NONE',  ( 0.000000000000000000, 1.496062992125984259, 0.000000000000000000 ) ) ;
#2835=LINE ( 'NONE', #2156, #5232 ) ;
#2846=ADVANCED_FACE ( 'NONE', ( #3254, #360 ), #480, .F. ) ;
#2881=CARTESIAN_POINT ( 'NONE',  ( 2.755905511811024056, 0.000000000000000000, -0.7480314960629921295 ) ) ;
#2912=SHAPE_REPRESENTATION ( 'Supporter', ( #5166 ), #879 ) ;
#2917=DIRECTION ( 'NONE',  ( -0.000000000000000000, -1.000000000000000000, -0.000000000000000000 ) ) ;
#2929=EDGE_CURVE ( 'NONE', #2163, #1565, #750, .T. ) ;
#2995=CARTESIAN_POINT ( 'NONE',  ( 0.000000000000000000, 1.496062992125984259, 0.000000000000000000 ) ) ;
#2997=PRODUCT_DEFINITION_SHAPE ( 'NONE', 'NONE',  #5662 ) ;
#3038=AXIS2_PLACEMENT_3D ( 'NONE', #6283, #5025, #4453 ) ;
#3068=AXIS2_PLACEMENT_3D ( 'NONE', #4740, #1831, #2491 ) ;
#3078=ADVANCED_FACE ( 'NONE', ( #6651 ), #155, .T. ) ;
#3103=EDGE_LOOP ( 'NONE', ( #3996, #5887 ) ) ;
#3154=VECTOR ( 'NONE', #838, 39.37007874015748143 ) ;
#3203=CARTESIAN_POINT ( 'NONE',  ( 0.000000000000000000, 0.000000000000000000, -0.7480314960629921295 ) ) ;
#3232=EDGE_CURVE ( 'NONE', #4990, #1208, #4132, .T. ) ;
#3254=FACE_BOUND ( 'NONE', #3103, .T. ) ;
#3270=EDGE_CURVE ( 'NONE', #1565, #1607, #5188, .T. ) ;
#3289=VECTOR ( 'NONE', #1139, 39.37007874015748143 ) ;
#3295=DIRECTION ( 'NONE',  ( 0.000000000000000000, 1.000000000000000000, 0.000000000000000000 ) ) ;
#3297=CARTESIAN_POINT ( 'NONE',  ( 1.850393700787401619, 0.7480314960629921295, -0.7480314960629921295 ) ) ;
#3312=DIRECTION ( 'NONE',  ( 0.000000000000000000, 0.000000000000000000, 1.000000000000000000 ) ) ;
#3336=AXIS2_PLACEMENT_3D ( 'NONE', #2205, #1017, #2247 ) ;
#3340=CARTESIAN_POINT ( 'NONE',  ( 2.755905511811024056, 1.496062992125984259, 0.7480314960629921295 ) ) ;
#3358=ORIENTED_EDGE ( 'NONE', *, *, #7320, .T. ) ;
#3359=UNCERTAINTY_MEASURE_WITH_UNIT (LENGTH_MEASURE( 1.000000000000000082E-05 ), #1271, 'distance_accuracy_value', 'NONE');
#3400=VECTOR ( 'NONE', #5647, 39.37007874015748143 ) ;
#3406=DIRECTION ( 'NONE',  ( -0.000000000000000000, -1.000000000000000000, -0.000000000000000000 ) ) ;
#3413=EDGE_CURVE ( 'NONE', #813, #2163, #6469, .T. ) ;
#3424=DIRECTION ( 'NONE',  ( 0.000000000000000000, -0.000000000000000000, 1.000000000000000000 ) ) ;
#3426=CARTESIAN_POINT ( 'NONE',  ( 0.000000000000000000, 1.496062992125984259, -0.7480314960629921295 ) ) ;
#3442=CARTESIAN_POINT ( 'NONE',  ( 0.000000000000000000, 1.496062992125984259, 0.000000000000000000 ) ) ;
#3458=DIRECTION ( 'NONE',  ( 0.000000000000000000, 1.000000000000000000, 0.000000000000000000 ) ) ;
#3480=ORIENTED_EDGE ( 'NONE', *, *, #604, .T. ) ;
#3487=ORIENTED_EDGE ( 'NONE', *, *, #4071, .T. ) ;
#3488=LINE ( 'NONE', #4000, #432 ) ;
#3493=CARTESIAN_POINT ( 'NONE',  ( 0.9055118110236223261, 0.7480314960629921295, 0.7480314960629921295 ) ) ;
#3517=DIRECTION ( 'NONE',  ( -1.000000000000000000, -0.000000000000000000, -0.000000000000000000 ) ) ;
#3523=PLANE ( 'NONE',  #5774 ) ;
#3533=VECTOR ( 'NONE', #5033, 39.37007874015748143 ) ;
#3538=LINE ( 'NONE', #2310, #2718 ) ;
#3566=FACE_OUTER_BOUND ( 'NONE', #4019, .T. ) ;
#3579=( NAMED_UNIT ( * ) PLANE_ANGLE_UNIT ( ) SI_UNIT ( $, .RADIAN. ) );
#3596=CIRCLE ( 'NONE', #2619, 0.4724409448818896462 ) ;
#3597=CARTESIAN_POINT ( 'NONE',  ( 0.000000000000000000, 1.496062992125984259, -0.7480314960629921295 ) ) ;
#3614=PRODUCT ( 'Supporter', 'Supporter', '', ( #5366 ) ) ;
#3634=EDGE_CURVE ( 'NONE', #2767, #4636, #609, .T. ) ;
#3641=ORIENTED_EDGE ( 'NONE', *, *, #793, .T. ) ;
#3647=CARTESIAN_POINT ( 'NONE',  ( 2.755905511811024056, 0.000000000000000000, 0.7480314960629921295 ) ) ;
#3649=ADVANCED_FACE ( 'NONE', ( #5040 ), #944, .F. ) ;
#3705=DIRECTION ( 'NONE',  ( 0.000000000000000000, 1.000000000000000000, 0.000000000000000000 ) ) ;
#3730=ORIENTED_EDGE ( 'NONE', *, *, #1078, .F. ) ;
#3751=EDGE_LOOP ( 'NONE', ( #124, #5097, #3911, #6468 ) ) ;
#3774=ADVANCED_BREP_SHAPE_REPRESENTATION ( '', ( #1517, #5166 ), #879 ) ;
#3785=ADVANCED_FACE ( 'NONE', ( #1659, #531 ), #1114, .F. ) ;
#3804=DIRECTION ( 'NONE',  ( 0.000000000000000000, 0.000000000000000000, 1.000000000000000000 ) ) ;
#3867=APPLICATION_CONTEXT ( 'automotive_design' ) ;
#3881=ORIENTED_EDGE ( 'NONE', *, *, #4716, .F. ) ;
#3885=AXIS2_PLACEMENT_3D ( 'NONE', #6354, #3295, #518 ) ;
#3911=ORIENTED_EDGE ( 'NONE', *, *, #4071, .F. ) ;
#3939=VECTOR ( 'NONE', #5451, 39.37007874015748143 ) ;
#3940=DIRECTION ( 'NONE',  ( 0.000000000000000000, 1.000000000000000000, 0.000000000000000000 ) ) ;
#3947=ORIENTED_EDGE ( 'NONE', *, *, #1494, .F. ) ;
#3959=EDGE_LOOP ( 'NONE', ( #1410, #4371, #3480, #5822 ) ) ;
#3963=ORIENTED_EDGE ( 'NONE', *, *, #7428, .T. ) ;
#3979=ORIENTED_EDGE ( 'NONE', *, *, #4716, .T. ) ;
#3996=ORIENTED_EDGE ( 'NONE', *, *, #565, .F. ) ;
#4000=CARTESIAN_POINT ( 'NONE',  ( 2.755905511811024056, 1.496062992125984259, -0.2362204724409449896 ) ) ;
#4019=EDGE_LOOP ( 'NONE', ( #3730, #5376, #5021, #7346 ) ) ;
#4024=ORIENTED_EDGE ( 'NONE', *, *, #1863, .T. ) ;
#4064=CIRCLE ( 'NONE', #5546, 0.7480314960629921295 ) ;
#4071=EDGE_CURVE ( 'NONE', #4636, #2767, #825, .T. ) ;
#4074=( LENGTH_UNIT ( ) NAMED_UNIT ( * ) SI_UNIT ( $, .METRE. ) );
#4082=DIRECTION ( 'NONE',  ( 0.000000000000000000, 0.000000000000000000, 1.000000000000000000 ) ) ;
#4086=CARTESIAN_POINT ( 'NONE',  ( 2.755905511811024056, 1.496062992125984259, 0.2362204724409449896 ) ) ;
#4116=DIRECTION ( 'NONE',  ( 0.000000000000000000, 1.000000000000000000, 0.000000000000000000 ) ) ;
#4132=LINE ( 'NONE', #1722, #3289 ) ;
#4134=FACE_OUTER_BOUND ( 'NONE', #6958, .T. ) ;
#4153=CARTESIAN_POINT ( 'NONE',  ( 1.850393700787401619, 0.7480314960629921295, 0.7480314960629921295 ) ) ;
#4158=DIRECTION ( 'NONE',  ( 0.000000000000000000, 0.000000000000000000, -1.000000000000000000 ) ) ;
#4164=EDGE_CURVE ( 'NONE', #6698, #813, #5316, .T. ) ;
#4176=EDGE_LOOP ( 'NONE', ( #5540, #5717, #4024, #6414 ) ) ;
#4184=EDGE_LOOP ( 'NONE', ( #3979, #5369 ) ) ;
#4197=CARTESIAN_POINT ( 'NONE',  ( 2.755905511811024056, 1.496062992125984259, 0.000000000000000000 ) ) ;
#4202=DIRECTION ( 'NONE',  ( 0.000000000000000000, 0.000000000000000000, -1.000000000000000000 ) ) ;
#4219=EDGE_LOOP ( 'NONE', ( #7176, #3947, #965, #7160 ) ) ;
#4253=CARTESIAN_POINT ( 'NONE',  ( 0.000000000000000000, 1.496062992125984259, -0.2362204724409449341 ) ) ;
#4264=AXIS2_PLACEMENT_3D ( 'NONE', #3442, #3406, #1678 ) ;
#4317=CARTESIAN_POINT ( 'NONE',  ( 0.000000000000000000, 1.496062992125984259, 0.7480314960629921295 ) ) ;
#4325=MECHANICAL_DESIGN_GEOMETRIC_PRESENTATION_REPRESENTATION('',(#6036),#7248);
#4339=ORIENTED_EDGE ( 'NONE', *, *, #882, .T. ) ;
#4371=ORIENTED_EDGE ( 'NONE', *, *, #6696, .T. ) ;
#4374=AXIS2_PLACEMENT_3D ( 'NONE', #723, #6047, #4929 ) ;
#4382=DIRECTION ( 'NONE',  ( -0.000000000000000000, -0.000000000000000000, 1.000000000000000000 ) ) ;
#4417=AXIS2_PLACEMENT_3D ( 'NONE', #7221, #1996, #4440 ) ;
#4440=DIRECTION ( 'NONE',  ( 0.000000000000000000, 0.000000000000000000, -1.000000000000000000 ) ) ;
#4441=SHAPE_DEFINITION_REPRESENTATION ( #2997, #2912 ) ;
#4442=AXIS2_PLACEMENT_3D ( 'NONE', #2812, #6870, #3312 ) ;
#4453=DIRECTION ( 'NONE',  ( -1.000000000000000000, 0.000000000000000000, -0.000000000000000000 ) ) ;
#4481=DIRECTION ( 'NONE',  ( 0.000000000000000000, 1.000000000000000000, 0.000000000000000000 ) ) ;
#4492=ORIENTED_EDGE ( 'NONE', *, *, #6696, .F. ) ;
#4539=EDGE_CURVE ( 'NONE', #7188, #139, #1934, .T. ) ;
#4540=CIRCLE ( 'NONE', #386, 0.2362204724409449896 ) ;
#4558=CARTESIAN_POINT ( 'NONE',  ( 0.000000000000000000, 0.000000000000000000, 0.000000000000000000 ) ) ;
#4619=DIRECTION ( 'NONE',  ( 0.000000000000000000, 0.000000000000000000, 1.000000000000000000 ) ) ;
#4636=VERTEX_POINT ( 'NONE', #5470 ) ;
#4649=DIRECTION ( 'NONE',  ( 0.000000000000000000, 0.000000000000000000, 1.000000000000000000 ) ) ;
#4705=DIRECTION ( 'NONE',  ( -0.000000000000000000, -0.000000000000000000, 1.000000000000000000 ) ) ;
#4716=EDGE_CURVE ( 'NONE', #7498, #2124, #7051, .T. ) ;
#4731=DIRECTION ( 'NONE',  ( 1.000000000000000000, 0.000000000000000000, 0.000000000000000000 ) ) ;
#4740=CARTESIAN_POINT ( 'NONE',  ( 1.377952755905512028, 0.7480314960629921295, -0.7480314960629921295 ) ) ;
#4761=DIRECTION ( 'NONE',  ( -0.000000000000000000, -1.000000000000000000, -0.000000000000000000 ) ) ;
#4794=DIRECTION ( 'NONE',  ( -0.000000000000000000, -1.000000000000000000, -0.000000000000000000 ) ) ;
#4809=UNCERTAINTY_MEASURE_WITH_UNIT (LENGTH_MEASURE( 1.000000000000000082E-05 ), #5297, 'distance_accuracy_value', 'NONE');
#4813=DIRECTION ( 'NONE',  ( 0.000000000000000000, 0.000000000000000000, 1.000000000000000000 ) ) ;
#4856=VECTOR ( 'NONE', #3517, 39.37007874015748143 ) ;
#4882=DIRECTION ( 'NONE',  ( -0.000000000000000000, -1.000000000000000000, -0.000000000000000000 ) ) ;
#4910=AXIS2_PLACEMENT_3D ( 'NONE', #6363, #4705, #1175 ) ;
#4929=DIRECTION ( 'NONE',  ( 0.000000000000000000, 0.000000000000000000, 1.000000000000000000 ) ) ;
#4990=VERTEX_POINT ( 'NONE', #2881 ) ;
#4998=CARTESIAN_POINT ( 'NONE',  ( 1.377952755905512028, 0.7480314960629921295, -0.7480314960629921295 ) ) ;
#5003=EDGE_CURVE ( 'NONE', #6730, #2124, #3538, .T. ) ;
#5021=ORIENTED_EDGE ( 'NONE', *, *, #7378, .T. ) ;
#5025=DIRECTION ( 'NONE',  ( 0.000000000000000000, 0.000000000000000000, -1.000000000000000000 ) ) ;
#5033=DIRECTION ( 'NONE',  ( 1.000000000000000000, 0.000000000000000000, 0.000000000000000000 ) ) ;
#5040=FACE_OUTER_BOUND ( 'NONE', #4176, .T. ) ;
#5064=VECTOR ( 'NONE', #4761, 39.37007874015748143 ) ;
#5066=EDGE_LOOP ( 'NONE', ( #2490, #6178 ) ) ;
#5067=DIRECTION ( 'NONE',  ( -0.000000000000000000, -1.000000000000000000, -0.000000000000000000 ) ) ;
#5074=DIMENSIONAL_EXPONENTS ( 1.000000000000000000, 0.000000000000000000, 0.000000000000000000, 0.000000000000000000, 0.000000000000000000, 0.000000000000000000, 0.000000000000000000 ) ;
#5097=ORIENTED_EDGE ( 'NONE', *, *, #1811, .T. ) ;
#5166=AXIS2_PLACEMENT_3D ( 'NONE', #418, #2134, #2741 ) ;
#5188=LINE ( 'NONE', #933, #3533 ) ;
#5215=DIMENSIONAL_EXPONENTS ( 1.000000000000000000, 0.000000000000000000, 0.000000000000000000, 0.000000000000000000, 0.000000000000000000, 0.000000000000000000, 0.000000000000000000 ) ;
#5232=VECTOR ( 'NONE', #5067, 39.37007874015748143 ) ;
#5269=CARTESIAN_POINT ( 'NONE',  ( 1.377952755905512028, 0.7480314960629921295, -0.7480314960629921295 ) ) ;
#5297=( CONVERSION_BASED_UNIT ( 'INCH', #7015 ) LENGTH_UNIT ( ) NAMED_UNIT ( #5215 ) );
#5298=CIRCLE ( 'NONE', #2738, 0.7480314960629921295 ) ;
#5314=ORIENTED_EDGE ( 'NONE', *, *, #2929, .F. ) ;
#5316=LINE ( 'NONE', #3597, #4856 ) ;
#5331=DIRECTION ( 'NONE',  ( -0.000000000000000000, -1.000000000000000000, -0.000000000000000000 ) ) ;
#5352=ORIENTED_EDGE ( 'NONE', *, *, #604, .F. ) ;
#5366=PRODUCT_CONTEXT ( 'NONE', #3867, 'mechanical' ) ;
#5369=ORIENTED_EDGE ( 'NONE', *, *, #5891, .T. ) ;
#5376=ORIENTED_EDGE ( 'NONE', *, *, #5762, .T. ) ;
#5394=DIRECTION ( 'NONE',  ( -0.000000000000000000, -1.000000000000000000, -0.000000000000000000 ) ) ;
#5410=ORIENTED_EDGE ( 'NONE', *, *, #2072, .F. ) ;
#5451=DIRECTION ( 'NONE',  ( -0.000000000000000000, -1.000000000000000000, -0.000000000000000000 ) ) ;
#5463=ORIENTED_EDGE ( 'NONE', *, *, #4539, .T. ) ;
#5470=CARTESIAN_POINT ( 'NONE',  ( 0.000000000000000000, 0.000000000000000000, -0.2362204724409449341 ) ) ;
#5492=LINE ( 'NONE', #4253, #3939 ) ;
#5510=DIRECTION ( 'NONE',  ( -0.000000000000000000, -1.000000000000000000, -0.000000000000000000 ) ) ;
#5517=EDGE_LOOP ( 'NONE', ( #1295, #5314, #2402, #5916 ) ) ;
#5519=FACE_OUTER_BOUND ( 'NONE', #5517, .T. ) ;
#5540=ORIENTED_EDGE ( 'NONE', *, *, #5762, .F. ) ;
#5546=AXIS2_PLACEMENT_3D ( 'NONE', #4558, #4481, #2753 ) ;
#5577=EDGE_CURVE ( 'NONE', #1208, #1565, #4064, .T. ) ;
#5618=CARTESIAN_POINT ( 'NONE',  ( 0.000000000000000000, 1.496062992125984259, 0.000000000000000000 ) ) ;
#5619=CARTESIAN_POINT ( 'NONE',  ( 0.000000000000000000, 0.000000000000000000, 0.000000000000000000 ) ) ;
#5644=ORIENTED_EDGE ( 'NONE', *, *, #5003, .T. ) ;
#5647=DIRECTION ( 'NONE',  ( -0.000000000000000000, -0.000000000000000000, 1.000000000000000000 ) ) ;
#5661=PLANE ( 'NONE',  #3336 ) ;
#5662=PRODUCT_DEFINITION ( 'UNKNOWN', '', #935, #754 ) ;
#5717=ORIENTED_EDGE ( 'NONE', *, *, #4539, .F. ) ;
#5737=CARTESIAN_POINT ( 'NONE',  ( 0.000000000000000000, 1.496062992125984259, -0.2362204724409449341 ) ) ;
#5742=VECTOR ( 'NONE', #4882, 39.37007874015748143 ) ;
#5746=ORIENTED_EDGE ( 'NONE', *, *, #1078, .T. ) ;
#5747=FACE_OUTER_BOUND ( 'NONE', #6312, .T. ) ;
#5760=FACE_BOUND ( 'NONE', #6640, .T. ) ;
#5762=EDGE_CURVE ( 'NONE', #139, #1597, #7288, .T. ) ;
#5774=AXIS2_PLACEMENT_3D ( 'NONE', #5863, #3458, #3424 ) ;
#5814=ORIENTED_EDGE ( 'NONE', *, *, #2929, .T. ) ;
#5822=ORIENTED_EDGE ( 'NONE', *, *, #5891, .F. ) ;
#5863=CARTESIAN_POINT ( 'NONE',  ( 0.000000000000000000, 1.496062992125984259, 0.000000000000000000 ) ) ;
#5876=CIRCLE ( 'NONE', #6974, 0.4724409448818896462 ) ;
#5887=ORIENTED_EDGE ( 'NONE', *, *, #7378, .F. ) ;
#5891=EDGE_CURVE ( 'NONE', #2124, #7498, #1234, .T. ) ;
#5916=ORIENTED_EDGE ( 'NONE', *, *, #1961, .T. ) ;
#5941=VERTEX_POINT ( 'NONE', #1551 ) ;
#5965=CARTESIAN_POINT ( 'NONE',  ( 2.755905511811024056, 0.000000000000000000, 0.2362204724409449896 ) ) ;
#6009=EDGE_LOOP ( 'NONE', ( #2194, #1401, #2505, #7348 ) ) ;
#6014=AXIS2_PLACEMENT_3D ( 'NONE', #4197, #4116, #4082 ) ;
#6036=STYLED_ITEM('',(#7594),#1517);
#6040=CARTESIAN_POINT ( 'NONE',  ( 0.000000000000000000, 1.496062992125984259, 0.7480314960629921295 ) ) ;
#6044=DIRECTION ( 'NONE',  ( 0.000000000000000000, 0.000000000000000000, 1.000000000000000000 ) ) ;
#6047=DIRECTION ( 'NONE',  ( 0.000000000000000000, 1.000000000000000000, 0.000000000000000000 ) ) ;
#6178=ORIENTED_EDGE ( 'NONE', *, *, #6353, .F. ) ;
#6205=DIRECTION ( 'NONE',  ( -0.000000000000000000, -1.000000000000000000, -0.000000000000000000 ) ) ;
#6221=FACE_OUTER_BOUND ( 'NONE', #6009, .T. ) ;
#6242=AXIS2_PLACEMENT_3D ( 'NONE', #2048, #6709, #3804 ) ;
#6247=CARTESIAN_POINT ( 'NONE',  ( 0.000000000000000000, 1.496062992125984259, -0.7480314960629921295 ) ) ;
#6283=CARTESIAN_POINT ( 'NONE',  ( 0.000000000000000000, 1.496062992125984259, 0.7480314960629921295 ) ) ;
#6307=ORIENTED_EDGE ( 'NONE', *, *, #1494, .T. ) ;
#6312=EDGE_LOOP ( 'NONE', ( #7264, #2575, #3641, #466 ) ) ;
#6353=EDGE_CURVE ( 'NONE', #1333, #1455, #173, .T. ) ;
#6354=CARTESIAN_POINT ( 'NONE',  ( 0.000000000000000000, 0.000000000000000000, 0.000000000000000000 ) ) ;
#6363=CARTESIAN_POINT ( 'NONE',  ( 1.377952755905512028, 0.7480314960629921295, -0.7480314960629921295 ) ) ;
#6366=ADVANCED_FACE ( 'NONE', ( #6221, #980, #7469 ), #5661, .F. ) ;
#6371=CIRCLE ( 'NONE', #6014, 0.7480314960629921295 ) ;
#6372=CIRCLE ( 'NONE', #3068, 0.4724409448818896462 ) ;
#6397=CARTESIAN_POINT ( 'NONE',  ( 1.377952755905512028, 0.7480314960629921295, 0.7480314960629921295 ) ) ;
#6409=DIRECTION ( 'NONE',  ( 0.000000000000000000, 1.000000000000000000, 0.000000000000000000 ) ) ;
#6411=DIRECTION ( 'NONE',  ( 1.000000000000000000, 0.000000000000000000, 0.000000000000000000 ) ) ;
#6414=ORIENTED_EDGE ( 'NONE', *, *, #565, .T. ) ;
#6443=( NAMED_UNIT ( * ) SI_UNIT ( $, .STERADIAN. ) SOLID_ANGLE_UNIT ( ) );
#6468=ORIENTED_EDGE ( 'NONE', *, *, #793, .F. ) ;
#6469=CIRCLE ( 'NONE', #257, 0.7480314960629921295 ) ;
#6482=CIRCLE ( 'NONE', #6242, 0.2362204724409449896 ) ;
#6507=EDGE_CURVE ( 'NONE', #1455, #1333, #756, .T. ) ;
#6527=( NAMED_UNIT ( * ) SI_UNIT ( $, .STERADIAN. ) SOLID_ANGLE_UNIT ( ) );
#6528=CLOSED_SHELL ( 'NONE', ( #615, #794, #2806, #652, #6366, #7057, #2846, #3078, #3785, #2280, #2022, #3649 ) ) ;
#6578=EDGE_LOOP ( 'NONE', ( #5463, #5746 ) ) ;
#6605=LINE ( 'NONE', #101, #5064 ) ;
#6630=AXIS2_PLACEMENT_3D ( 'NONE', #1630, #3940, #6882 ) ;
#6640=EDGE_LOOP ( 'NONE', ( #7085, #4492 ) ) ;
#6651=FACE_OUTER_BOUND ( 'NONE', #4219, .T. ) ;
#6682=CARTESIAN_POINT ( 'NONE',  ( 2.755905511811024056, 0.000000000000000000, -0.2362204724409449896 ) ) ;
#6696=EDGE_CURVE ( 'NONE', #6730, #5941, #6482, .T. ) ;
#6698=VERTEX_POINT ( 'NONE', #899 ) ;
#6709=DIRECTION ( 'NONE',  ( 0.000000000000000000, 1.000000000000000000, 0.000000000000000000 ) ) ;
#6724=CARTESIAN_POINT ( 'NONE',  ( 0.9055118110236223261, 0.7480314960629921295, -0.7480314960629921295 ) ) ;
#6730=VERTEX_POINT ( 'NONE', #4086 ) ;
#6742=VECTOR ( 'NONE', #444, 39.37007874015748143 ) ;
#6870=DIRECTION ( 'NONE',  ( 0.000000000000000000, 1.000000000000000000, 0.000000000000000000 ) ) ;
#6882=DIRECTION ( 'NONE',  ( 0.000000000000000000, 0.000000000000000000, 1.000000000000000000 ) ) ;
#6936=ORIENTED_EDGE ( 'NONE', *, *, #3270, .T. ) ;
#6941=DIRECTION ( 'NONE',  ( 0.000000000000000000, 1.000000000000000000, 0.000000000000000000 ) ) ;
#6958=EDGE_LOOP ( 'NONE', ( #1446, #4339, #3358, #2324 ) ) ;
#6974=AXIS2_PLACEMENT_3D ( 'NONE', #151, #4813, #6411 ) ;
#6979=AXIS2_PLACEMENT_3D ( 'NONE', #2995, #6941, #1697 ) ;
#7003=DIRECTION ( 'NONE',  ( 1.000000000000000000, 0.000000000000000000, 0.000000000000000000 ) ) ;
#7015=LENGTH_MEASURE_WITH_UNIT ( LENGTH_MEASURE( 0.02539999999999999897 ), #4074 );
#7051=CIRCLE ( 'NONE', #4374, 0.2362204724409449896 ) ;
#7057=ADVANCED_FACE ( 'NONE', ( #5519 ), #7180, .T. ) ;
#7059=CARTESIAN_POINT ( 'NONE',  ( 2.755905511811024056, 0.000000000000000000, 0.000000000000000000 ) ) ;
#7085=ORIENTED_EDGE ( 'NONE', *, *, #7428, .F. ) ;
#7160=ORIENTED_EDGE ( 'NONE', *, *, #2072, .T. ) ;
#7176=ORIENTED_EDGE ( 'NONE', *, *, #329, .T. ) ;
#7180=CYLINDRICAL_SURFACE ( 'NONE', #4417, 0.7480314960629921295 ) ;
#7185=ORIENTED_EDGE ( 'NONE', *, *, #1961, .F. ) ;
#7188=VERTEX_POINT ( 'NONE', #2179 ) ;
#7190=AXIS2_PLACEMENT_3D ( 'NONE', #7454, #6205, #1489 ) ;
#7211=CARTESIAN_POINT ( 'NONE',  ( 2.755905511811024056, 1.496062992125984259, 0.000000000000000000 ) ) ;
#7213=CYLINDRICAL_SURFACE ( 'NONE', #2062, 0.2362204724409449896 ) ;
#7221=CARTESIAN_POINT ( 'NONE',  ( 0.000000000000000000, 1.496062992125984259, 0.000000000000000000 ) ) ;
#7232=CARTESIAN_POINT ( 'NONE',  ( 2.755905511811024056, 1.496062992125984259, 0.000000000000000000 ) ) ;
#7248=( GEOMETRIC_REPRESENTATION_CONTEXT ( 3 ) GLOBAL_UNCERTAINTY_ASSIGNED_CONTEXT ( ( #3359 ) ) GLOBAL_UNIT_ASSIGNED_CONTEXT ( ( #1271, #3579, #6443 ) ) REPRESENTATION_CONTEXT ( 'NONE', 'WORKASPACE' ) );
#7264=ORIENTED_EDGE ( 'NONE', *, *, #1811, .F. ) ;
#7288=LINE ( 'NONE', #6724, #1011 ) ;
#7320=EDGE_CURVE ( 'NONE', #1804, #6698, #6371, .T. ) ;
#7346=ORIENTED_EDGE ( 'NONE', *, *, #1863, .F. ) ;
#7348=ORIENTED_EDGE ( 'NONE', *, *, #3270, .F. ) ;
#7376=VERTEX_POINT ( 'NONE', #4153 ) ;
#7378=EDGE_CURVE ( 'NONE', #1597, #7376, #5876, .T. ) ;
#7405=ORIENTED_EDGE ( 'NONE', *, *, #3232, .T. ) ;
#7428=EDGE_CURVE ( 'NONE', #5941, #6730, #4540, .T. ) ;
#7454=CARTESIAN_POINT ( 'NONE',  ( 0.000000000000000000, 1.496062992125984259, 0.000000000000000000 ) ) ;
#7469=FACE_BOUND ( 'NONE', #4184, .T. ) ;
#7498=VERTEX_POINT ( 'NONE', #6682 ) ;
#7588=COLOUR_RGB('Off White',0.89,0.88,0.83);
#7589=FILL_AREA_STYLE_COLOUR('',#7588);
#7590=FILL_AREA_STYLE('',(#7589));
#7591=SURFACE_STYLE_FILL_AREA(#7590);
#7592=SURFACE_SIDE_STYLE('',(#7591));
#7593=SURFACE_STYLE_USAGE(.BOTH.,#7592);
#7594=PRESENTATION_STYLE_ASSIGNMENT((#7593));
ENDSEC;
END-ISO-10303-21;
